ISO-10303-21;
HEADER;
/* Generated by software containing ST-Developer
 * from STEP Tools, Inc. (www.steptools.com) 
 */

FILE_DESCRIPTION(
/* description */ ('Compact handwheel screw vise'),
/* implementation_level */ '2;1');

FILE_NAME(
/* name */ 'Cap Screw - M6x25.step',
/* time_stamp */ '2026-10-29T16:08:22-07:00',
/* author */ (''),
/* organization */ (''),
/* preprocessor_version */ 'ST-DEVELOPER v20.2',
/* originating_system */ 'Autodesk Translation Framework v15.17.0.0',
/* authorisation */ '');

FILE_SCHEMA (('AUTOMOTIVE_DESIGN { 1 0 10303 214 3 1 1 }'));
ENDSEC;

DATA;
#10=MECHANICAL_DESIGN_GEOMETRIC_PRESENTATION_REPRESENTATION('',(#679),#25074);
#576=CONICAL_SURFACE('',#9148,0.475,0.785398163397449);
#577=CONICAL_SURFACE('',#9152,0.485,0.785398163397448);
#578=CONICAL_SURFACE('',#9156,0.31,0.463647609000806);
#579=CONICAL_SURFACE('',#9160,0.27,0.785398163397448);
#583=ORIENTED_CLOSED_SHELL('',*,#8091,.F.);
#587=BREP_WITH_VOIDS('Body1',#8090,(#583));
#615=SHAPE_REPRESENTATION_RELATIONSHIP('SRR','None',#25226,#643);
#643=ADVANCED_BREP_SHAPE_REPRESENTATION('',(#587),#25073);
#679=STYLED_ITEM('',(#25446),#587);
#821=FACE_BOUND('',#2049,.T.);
#1001=PLANE('',#9146);
#1002=PLANE('',#9154);
#1003=PLANE('',#9162);
#1004=PLANE('',#9163);
#1005=PLANE('',#9164);
#1006=PLANE('',#9165);
#1007=PLANE('',#9166);
#1008=PLANE('',#9167);
#1009=PLANE('',#9168);
#1010=PLANE('',#9169);
#1011=PLANE('',#9170);
#1465=FACE_OUTER_BOUND('',#2044,.T.);
#1466=FACE_OUTER_BOUND('',#2045,.T.);
#1467=FACE_OUTER_BOUND('',#2046,.T.);
#1468=FACE_OUTER_BOUND('',#2047,.T.);
#1469=FACE_OUTER_BOUND('',#2048,.T.);
#1470=FACE_OUTER_BOUND('',#2050,.T.);
#1471=FACE_OUTER_BOUND('',#2051,.T.);
#1472=FACE_OUTER_BOUND('',#2052,.T.);
#1473=FACE_OUTER_BOUND('',#2053,.T.);
#1474=FACE_OUTER_BOUND('',#2054,.T.);
#1475=FACE_OUTER_BOUND('',#2055,.T.);
#1476=FACE_OUTER_BOUND('',#2056,.T.);
#1477=FACE_OUTER_BOUND('',#2057,.T.);
#1478=FACE_OUTER_BOUND('',#2058,.T.);
#1479=FACE_OUTER_BOUND('',#2059,.T.);
#1480=FACE_OUTER_BOUND('',#2060,.T.);
#1481=FACE_OUTER_BOUND('',#2061,.T.);
#2044=EDGE_LOOP('',(#7281));
#2045=EDGE_LOOP('',(#7282,#7283,#7284,#7285));
#2046=EDGE_LOOP('',(#7286,#7287,#7288,#7289));
#2047=EDGE_LOOP('',(#7290,#7291,#7292,#7293));
#2048=EDGE_LOOP('',(#7294));
#2049=EDGE_LOOP('',(#7295));
#2050=EDGE_LOOP('',(#7296,#7297,#7298,#7299));
#2051=EDGE_LOOP('',(#7300,#7301,#7302,#7303));
#2052=EDGE_LOOP('',(#7304,#7305,#7306,#7307));
#2053=EDGE_LOOP('',(#7308));
#2054=EDGE_LOOP('',(#7309,#7310,#7311,#7312));
#2055=EDGE_LOOP('',(#7313,#7314,#7315,#7316));
#2056=EDGE_LOOP('',(#7317,#7318,#7319,#7320));
#2057=EDGE_LOOP('',(#7321,#7322,#7323,#7324));
#2058=EDGE_LOOP('',(#7325,#7326,#7327,#7328));
#2059=EDGE_LOOP('',(#7329,#7330,#7331,#7332));
#2060=EDGE_LOOP('',(#7333,#7334,#7335,#7336,#7337,#7338));
#2061=EDGE_LOOP('',(#7339,#7340,#7341,#7342,#7343,#7344));
#2546=LINE('',#24911,#3054);
#2547=LINE('',#24915,#3055);
#2548=LINE('',#24919,#3056);
#2549=LINE('',#24926,#3057);
#2550=LINE('',#24930,#3058);
#2551=LINE('',#24934,#3059);
#2552=LINE('',#24939,#3060);
#2553=LINE('',#24941,#3061);
#2554=LINE('',#24943,#3062);
#2555=LINE('',#24944,#3063);
#2556=LINE('',#24947,#3064);
#2557=LINE('',#24949,#3065);
#2558=LINE('',#24950,#3066);
#2559=LINE('',#24953,#3067);
#2560=LINE('',#24955,#3068);
#2561=LINE('',#24956,#3069);
#2562=LINE('',#24959,#3070);
#2563=LINE('',#24961,#3071);
#2564=LINE('',#24962,#3072);
#2565=LINE('',#24965,#3073);
#2566=LINE('',#24967,#3074);
#2567=LINE('',#24968,#3075);
#2568=LINE('',#24970,#3076);
#2569=LINE('',#24971,#3077);
#3054=VECTOR('',#11186,0.475);
#3055=VECTOR('',#11191,0.5);
#3056=VECTOR('',#11196,0.485);
#3057=VECTOR('',#11205,0.31);
#3058=VECTOR('',#11210,0.3);
#3059=VECTOR('',#11215,0.27);
#3060=VECTOR('',#11220,1.);
#3061=VECTOR('',#11221,1.);
#3062=VECTOR('',#11222,1.);
#3063=VECTOR('',#11223,1.);
#3064=VECTOR('',#11226,1.);
#3065=VECTOR('',#11227,1.);
#3066=VECTOR('',#11228,1.);
#3067=VECTOR('',#11231,1.);
#3068=VECTOR('',#11232,1.);
#3069=VECTOR('',#11233,1.);
#3070=VECTOR('',#11236,1.);
#3071=VECTOR('',#11237,1.);
#3072=VECTOR('',#11238,1.);
#3073=VECTOR('',#11241,1.);
#3074=VECTOR('',#11242,1.);
#3075=VECTOR('',#11243,1.);
#3076=VECTOR('',#11246,1.);
#3077=VECTOR('',#11247,1.);
#3325=CIRCLE('',#9147,0.45);
#3326=CIRCLE('',#9149,0.5);
#3327=CIRCLE('',#9151,0.5);
#3328=CIRCLE('',#9153,0.47);
#3329=CIRCLE('',#9155,0.32);
#3330=CIRCLE('',#9157,0.2942);
#3331=CIRCLE('',#9159,0.2942);
#3332=CIRCLE('',#9161,0.24);
#4046=VERTEX_POINT('',#24906);
#4047=VERTEX_POINT('',#24909);
#4048=VERTEX_POINT('',#24913);
#4049=VERTEX_POINT('',#24917);
#4050=VERTEX_POINT('',#24921);
#4051=VERTEX_POINT('',#24924);
#4052=VERTEX_POINT('',#24928);
#4053=VERTEX_POINT('',#24932);
#4054=VERTEX_POINT('',#24937);
#4055=VERTEX_POINT('',#24938);
#4056=VERTEX_POINT('',#24940);
#4057=VERTEX_POINT('',#24942);
#4058=VERTEX_POINT('',#24946);
#4059=VERTEX_POINT('',#24948);
#4060=VERTEX_POINT('',#24952);
#4061=VERTEX_POINT('',#24954);
#4062=VERTEX_POINT('',#24958);
#4063=VERTEX_POINT('',#24960);
#4064=VERTEX_POINT('',#24964);
#4065=VERTEX_POINT('',#24966);
#5127=EDGE_CURVE('',#4046,#4046,#3325,.T.);
#5128=EDGE_CURVE('',#4047,#4047,#3326,.T.);
#5129=EDGE_CURVE('',#4047,#4046,#2546,.T.);
#5130=EDGE_CURVE('',#4048,#4048,#3327,.T.);
#5131=EDGE_CURVE('',#4048,#4047,#2547,.T.);
#5132=EDGE_CURVE('',#4049,#4049,#3328,.T.);
#5133=EDGE_CURVE('',#4049,#4048,#2548,.T.);
#5134=EDGE_CURVE('',#4050,#4050,#3329,.T.);
#5135=EDGE_CURVE('',#4051,#4051,#3330,.F.);
#5136=EDGE_CURVE('',#4051,#4050,#2549,.T.);
#5137=EDGE_CURVE('',#4052,#4052,#3331,.F.);
#5138=EDGE_CURVE('',#4052,#4051,#2550,.T.);
#5139=EDGE_CURVE('',#4053,#4053,#3332,.T.);
#5140=EDGE_CURVE('',#4053,#4052,#2551,.T.);
#5141=EDGE_CURVE('',#4054,#4055,#2552,.T.);
#5142=EDGE_CURVE('',#4055,#4056,#2553,.T.);
#5143=EDGE_CURVE('',#4056,#4057,#2554,.T.);
#5144=EDGE_CURVE('',#4054,#4057,#2555,.T.);
#5145=EDGE_CURVE('',#4055,#4058,#2556,.T.);
#5146=EDGE_CURVE('',#4058,#4059,#2557,.T.);
#5147=EDGE_CURVE('',#4059,#4056,#2558,.T.);
#5148=EDGE_CURVE('',#4058,#4060,#2559,.T.);
#5149=EDGE_CURVE('',#4060,#4061,#2560,.T.);
#5150=EDGE_CURVE('',#4061,#4059,#2561,.T.);
#5151=EDGE_CURVE('',#4060,#4062,#2562,.T.);
#5152=EDGE_CURVE('',#4062,#4063,#2563,.T.);
#5153=EDGE_CURVE('',#4063,#4061,#2564,.T.);
#5154=EDGE_CURVE('',#4062,#4064,#2565,.T.);
#5155=EDGE_CURVE('',#4064,#4065,#2566,.T.);
#5156=EDGE_CURVE('',#4065,#4063,#2567,.T.);
#5157=EDGE_CURVE('',#4064,#4054,#2568,.T.);
#5158=EDGE_CURVE('',#4057,#4065,#2569,.T.);
#7281=ORIENTED_EDGE('',*,*,#5127,.F.);
#7282=ORIENTED_EDGE('',*,*,#5128,.F.);
#7283=ORIENTED_EDGE('',*,*,#5129,.T.);
#7284=ORIENTED_EDGE('',*,*,#5127,.T.);
#7285=ORIENTED_EDGE('',*,*,#5129,.F.);
#7286=ORIENTED_EDGE('',*,*,#5130,.F.);
#7287=ORIENTED_EDGE('',*,*,#5131,.T.);
#7288=ORIENTED_EDGE('',*,*,#5128,.T.);
#7289=ORIENTED_EDGE('',*,*,#5131,.F.);
#7290=ORIENTED_EDGE('',*,*,#5132,.F.);
#7291=ORIENTED_EDGE('',*,*,#5133,.T.);
#7292=ORIENTED_EDGE('',*,*,#5130,.T.);
#7293=ORIENTED_EDGE('',*,*,#5133,.F.);
#7294=ORIENTED_EDGE('',*,*,#5132,.T.);
#7295=ORIENTED_EDGE('',*,*,#5134,.F.);
#7296=ORIENTED_EDGE('',*,*,#5135,.F.);
#7297=ORIENTED_EDGE('',*,*,#5136,.T.);
#7298=ORIENTED_EDGE('',*,*,#5134,.T.);
#7299=ORIENTED_EDGE('',*,*,#5136,.F.);
#7300=ORIENTED_EDGE('',*,*,#5137,.F.);
#7301=ORIENTED_EDGE('',*,*,#5138,.T.);
#7302=ORIENTED_EDGE('',*,*,#5135,.T.);
#7303=ORIENTED_EDGE('',*,*,#5138,.F.);
#7304=ORIENTED_EDGE('',*,*,#5139,.F.);
#7305=ORIENTED_EDGE('',*,*,#5140,.T.);
#7306=ORIENTED_EDGE('',*,*,#5137,.T.);
#7307=ORIENTED_EDGE('',*,*,#5140,.F.);
#7308=ORIENTED_EDGE('',*,*,#5139,.T.);
#7309=ORIENTED_EDGE('',*,*,#5141,.T.);
#7310=ORIENTED_EDGE('',*,*,#5142,.T.);
#7311=ORIENTED_EDGE('',*,*,#5143,.T.);
#7312=ORIENTED_EDGE('',*,*,#5144,.F.);
#7313=ORIENTED_EDGE('',*,*,#5145,.T.);
#7314=ORIENTED_EDGE('',*,*,#5146,.T.);
#7315=ORIENTED_EDGE('',*,*,#5147,.T.);
#7316=ORIENTED_EDGE('',*,*,#5142,.F.);
#7317=ORIENTED_EDGE('',*,*,#5148,.T.);
#7318=ORIENTED_EDGE('',*,*,#5149,.T.);
#7319=ORIENTED_EDGE('',*,*,#5150,.T.);
#7320=ORIENTED_EDGE('',*,*,#5146,.F.);
#7321=ORIENTED_EDGE('',*,*,#5151,.T.);
#7322=ORIENTED_EDGE('',*,*,#5152,.T.);
#7323=ORIENTED_EDGE('',*,*,#5153,.T.);
#7324=ORIENTED_EDGE('',*,*,#5149,.F.);
#7325=ORIENTED_EDGE('',*,*,#5154,.T.);
#7326=ORIENTED_EDGE('',*,*,#5155,.T.);
#7327=ORIENTED_EDGE('',*,*,#5156,.T.);
#7328=ORIENTED_EDGE('',*,*,#5152,.F.);
#7329=ORIENTED_EDGE('',*,*,#5157,.T.);
#7330=ORIENTED_EDGE('',*,*,#5144,.T.);
#7331=ORIENTED_EDGE('',*,*,#5158,.T.);
#7332=ORIENTED_EDGE('',*,*,#5155,.F.);
#7333=ORIENTED_EDGE('',*,*,#5157,.F.);
#7334=ORIENTED_EDGE('',*,*,#5154,.F.);
#7335=ORIENTED_EDGE('',*,*,#5151,.F.);
#7336=ORIENTED_EDGE('',*,*,#5148,.F.);
#7337=ORIENTED_EDGE('',*,*,#5145,.F.);
#7338=ORIENTED_EDGE('',*,*,#5141,.F.);
#7339=ORIENTED_EDGE('',*,*,#5158,.F.);
#7340=ORIENTED_EDGE('',*,*,#5143,.F.);
#7341=ORIENTED_EDGE('',*,*,#5147,.F.);
#7342=ORIENTED_EDGE('',*,*,#5150,.F.);
#7343=ORIENTED_EDGE('',*,*,#5153,.F.);
#7344=ORIENTED_EDGE('',*,*,#5156,.F.);
#7580=CYLINDRICAL_SURFACE('',#9150,0.5);
#7581=CYLINDRICAL_SURFACE('',#9158,0.2942);
#8035=ADVANCED_FACE('',(#1465),#1001,.T.);
#8036=ADVANCED_FACE('',(#1466),#576,.T.);
#8037=ADVANCED_FACE('',(#1467),#7580,.T.);
#8038=ADVANCED_FACE('',(#1468),#577,.T.);
#8039=ADVANCED_FACE('',(#1469,#821),#1002,.T.);
#8040=ADVANCED_FACE('',(#1470),#578,.T.);
#8041=ADVANCED_FACE('',(#1471),#7581,.T.);
#8042=ADVANCED_FACE('',(#1472),#579,.T.);
#8043=ADVANCED_FACE('',(#1473),#1003,.T.);
#8044=ADVANCED_FACE('',(#1474),#1004,.F.);
#8045=ADVANCED_FACE('',(#1475),#1005,.F.);
#8046=ADVANCED_FACE('',(#1476),#1006,.F.);
#8047=ADVANCED_FACE('',(#1477),#1007,.F.);
#8048=ADVANCED_FACE('',(#1478),#1008,.F.);
#8049=ADVANCED_FACE('',(#1479),#1009,.F.);
#8050=ADVANCED_FACE('',(#1480),#1010,.F.);
#8051=ADVANCED_FACE('',(#1481),#1011,.F.);
#8090=CLOSED_SHELL('',(#8035,#8036,#8037,#8038,#8039,#8040,#8041,#8042,
#8043));
#8091=CLOSED_SHELL('',(#8044,#8045,#8046,#8047,#8048,#8049,#8050,#8051));
#9145=AXIS2_PLACEMENT_3D('',#24904,#11176,#11177);
#9146=AXIS2_PLACEMENT_3D('',#24905,#11178,#11179);
#9147=AXIS2_PLACEMENT_3D('',#24907,#11180,#11181);
#9148=AXIS2_PLACEMENT_3D('',#24908,#11182,#11183);
#9149=AXIS2_PLACEMENT_3D('',#24910,#11184,#11185);
#9150=AXIS2_PLACEMENT_3D('',#24912,#11187,#11188);
#9151=AXIS2_PLACEMENT_3D('',#24914,#11189,#11190);
#9152=AXIS2_PLACEMENT_3D('',#24916,#11192,#11193);
#9153=AXIS2_PLACEMENT_3D('',#24918,#11194,#11195);
#9154=AXIS2_PLACEMENT_3D('',#24920,#11197,#11198);
#9155=AXIS2_PLACEMENT_3D('',#24922,#11199,#11200);
#9156=AXIS2_PLACEMENT_3D('',#24923,#11201,#11202);
#9157=AXIS2_PLACEMENT_3D('',#24925,#11203,#11204);
#9158=AXIS2_PLACEMENT_3D('',#24927,#11206,#11207);
#9159=AXIS2_PLACEMENT_3D('',#24929,#11208,#11209);
#9160=AXIS2_PLACEMENT_3D('',#24931,#11211,#11212);
#9161=AXIS2_PLACEMENT_3D('',#24933,#11213,#11214);
#9162=AXIS2_PLACEMENT_3D('',#24935,#11216,#11217);
#9163=AXIS2_PLACEMENT_3D('',#24936,#11218,#11219);
#9164=AXIS2_PLACEMENT_3D('',#24945,#11224,#11225);
#9165=AXIS2_PLACEMENT_3D('',#24951,#11229,#11230);
#9166=AXIS2_PLACEMENT_3D('',#24957,#11234,#11235);
#9167=AXIS2_PLACEMENT_3D('',#24963,#11239,#11240);
#9168=AXIS2_PLACEMENT_3D('',#24969,#11244,#11245);
#9169=AXIS2_PLACEMENT_3D('',#24972,#11248,#11249);
#9170=AXIS2_PLACEMENT_3D('',#24973,#11250,#11251);
#11176=DIRECTION('axis',(0.,0.,1.));
#11177=DIRECTION('refdir',(1.,0.,0.));
#11178=DIRECTION('center_axis',(0.,1.,0.));
#11179=DIRECTION('ref_axis',(0.,0.,1.));
#11180=DIRECTION('center_axis',(0.,-1.,0.));
#11181=DIRECTION('ref_axis',(1.,0.,0.));
#11182=DIRECTION('center_axis',(0.,-1.,0.));
#11183=DIRECTION('ref_axis',(1.,0.,0.));
#11184=DIRECTION('center_axis',(0.,-1.,0.));
#11185=DIRECTION('ref_axis',(1.,0.,0.));
#11186=DIRECTION('',(0.707106781186548,0.707106781186547,8.65956056235494E-17));
#11187=DIRECTION('center_axis',(0.,-1.,0.));
#11188=DIRECTION('ref_axis',(1.,0.,0.));
#11189=DIRECTION('center_axis',(0.,-1.,0.));
#11190=DIRECTION('ref_axis',(1.,0.,0.));
#11191=DIRECTION('',(0.,1.,0.));
#11192=DIRECTION('center_axis',(0.,1.,0.));
#11193=DIRECTION('ref_axis',(1.,0.,0.));
#11194=DIRECTION('center_axis',(0.,-1.,0.));
#11195=DIRECTION('ref_axis',(1.,0.,0.));
#11196=DIRECTION('',(-0.707106781186547,0.707106781186548,-8.65956056235493E-17));
#11197=DIRECTION('center_axis',(0.,-1.,0.));
#11198=DIRECTION('ref_axis',(0.,0.,-1.));
#11199=DIRECTION('center_axis',(0.,-1.,0.));
#11200=DIRECTION('ref_axis',(1.,0.,0.));
#11201=DIRECTION('center_axis',(0.,1.,0.));
#11202=DIRECTION('ref_axis',(1.,0.,0.));
#11203=DIRECTION('center_axis',(0.,1.,0.));
#11204=DIRECTION('ref_axis',(1.,0.,0.));
#11205=DIRECTION('',(-0.447213595499958,0.894427190999916,-5.47678698264203E-17));
#11206=DIRECTION('center_axis',(0.,-1.,0.));
#11207=DIRECTION('ref_axis',(1.,0.,0.));
#11208=DIRECTION('center_axis',(0.,1.,0.));
#11209=DIRECTION('ref_axis',(1.,0.,0.));
#11210=DIRECTION('',(0.,1.,0.));
#11211=DIRECTION('center_axis',(0.,1.,0.));
#11212=DIRECTION('ref_axis',(1.,0.,0.));
#11213=DIRECTION('center_axis',(0.,-1.,0.));
#11214=DIRECTION('ref_axis',(1.,0.,0.));
#11215=DIRECTION('',(-0.707106781186547,0.707106781186548,-8.65956056235493E-17));
#11216=DIRECTION('center_axis',(0.,-1.,0.));
#11217=DIRECTION('ref_axis',(0.,0.,-1.));
#11218=DIRECTION('center_axis',(0.866025403784439,0.,-0.5));
#11219=DIRECTION('ref_axis',(0.5,0.,0.866025403784439));
#11220=DIRECTION('',(-0.5,0.,-0.866025403784439));
#11221=DIRECTION('',(0.,-1.,0.));
#11222=DIRECTION('',(0.5,0.,0.866025403784439));
#11223=DIRECTION('',(0.,-1.,0.));
#11224=DIRECTION('center_axis',(1.92296268638356E-16,0.,-1.));
#11225=DIRECTION('ref_axis',(1.,0.,1.92296268638356E-16));
#11226=DIRECTION('',(-1.,0.,-1.92296268638356E-16));
#11227=DIRECTION('',(0.,-1.,0.));
#11228=DIRECTION('',(1.,0.,1.92296268638356E-16));
#11229=DIRECTION('center_axis',(-0.866025403784439,0.,-0.5));
#11230=DIRECTION('ref_axis',(0.5,0.,-0.866025403784439));
#11231=DIRECTION('',(-0.5,0.,0.866025403784438));
#11232=DIRECTION('',(0.,-1.,0.));
#11233=DIRECTION('',(0.5,0.,-0.866025403784438));
#11234=DIRECTION('center_axis',(-0.866025403784439,0.,0.5));
#11235=DIRECTION('ref_axis',(-0.5,0.,-0.866025403784439));
#11236=DIRECTION('',(0.5,0.,0.866025403784439));
#11237=DIRECTION('',(0.,-1.,0.));
#11238=DIRECTION('',(-0.5,0.,-0.866025403784439));
#11239=DIRECTION('center_axis',(-1.92296268638356E-16,0.,1.));
#11240=DIRECTION('ref_axis',(-1.,0.,-1.92296268638356E-16));
#11241=DIRECTION('',(1.,0.,1.92296268638356E-16));
#11242=DIRECTION('',(0.,-1.,0.));
#11243=DIRECTION('',(-1.,0.,-1.92296268638356E-16));
#11244=DIRECTION('center_axis',(0.866025403784439,0.,0.5));
#11245=DIRECTION('ref_axis',(-0.5,0.,0.866025403784439));
#11246=DIRECTION('',(0.5,0.,-0.866025403784439));
#11247=DIRECTION('',(-0.5,0.,0.866025403784439));
#11248=DIRECTION('center_axis',(0.,1.,0.));
#11249=DIRECTION('ref_axis',(1.,0.,0.));
#11250=DIRECTION('center_axis',(0.,-1.,0.));
#11251=DIRECTION('ref_axis',(0.,0.,-1.));
#24904=CARTESIAN_POINT('',(0.,0.,0.));
#24905=CARTESIAN_POINT('Origin',(0.45,0.6,0.));
#24906=CARTESIAN_POINT('',(-0.45,0.6,-5.51091059616309E-17));
#24907=CARTESIAN_POINT('Origin',(0.,0.6,0.));
#24908=CARTESIAN_POINT('Origin',(0.,0.575,0.));
#24909=CARTESIAN_POINT('',(-0.5,0.55,-6.12323399573677E-17));
#24910=CARTESIAN_POINT('Origin',(0.,0.55,0.));
#24911=CARTESIAN_POINT('',(-0.475,0.575,-5.81707229594993E-17));
#24912=CARTESIAN_POINT('Origin',(0.,0.29,0.));
#24913=CARTESIAN_POINT('',(-0.5,0.0299999999999998,-6.12323399573677E-17));
#24914=CARTESIAN_POINT('Origin',(0.,0.0299999999999998,0.));
#24915=CARTESIAN_POINT('',(-0.5,0.29,-6.12323399573677E-17));
#24916=CARTESIAN_POINT('Origin',(0.,0.0150000000000001,0.));
#24917=CARTESIAN_POINT('',(-0.47,7.11236625150491E-17,-5.75583995599256E-17));
#24918=CARTESIAN_POINT('Origin',(0.,0.,0.));
#24919=CARTESIAN_POINT('',(-0.485,0.0150000000000001,-5.93953697586466E-17));
#24920=CARTESIAN_POINT('Origin',(0.32,0.,0.));
#24921=CARTESIAN_POINT('',(-0.32,-6.93889390390723E-18,-3.91886975727153E-17));
#24922=CARTESIAN_POINT('Origin',(0.,0.,0.));
#24923=CARTESIAN_POINT('Origin',(0.,-0.02,0.));
#24924=CARTESIAN_POINT('',(-0.2942,-0.0515999999999999,3.60291088309151E-17));
#24925=CARTESIAN_POINT('Origin',(0.,-0.0515999999999999,0.));
#24926=CARTESIAN_POINT('',(-0.31,-0.02,-3.7964050773568E-17));
#24927=CARTESIAN_POINT('Origin',(0.,-1.24,0.));
#24928=CARTESIAN_POINT('',(-0.2942,-2.4458,3.60291088309151E-17));
#24929=CARTESIAN_POINT('Origin',(0.,-2.4458,0.));
#24930=CARTESIAN_POINT('',(-0.2942,-1.24,-3.60291088309151E-17));
#24931=CARTESIAN_POINT('Origin',(0.,-2.47,0.));
#24932=CARTESIAN_POINT('',(-0.24,-2.5,-2.93915231795365E-17));
#24933=CARTESIAN_POINT('Origin',(0.,-2.5,0.));
#24934=CARTESIAN_POINT('',(-0.27,-2.47,-3.30654635769785E-17));
#24935=CARTESIAN_POINT('Origin',(0.,-2.5,0.));
#24936=CARTESIAN_POINT('Origin',(0.144337567297406,-0.6,-0.25));
#24937=CARTESIAN_POINT('',(0.288675134594813,-0.6,0.));
#24938=CARTESIAN_POINT('',(0.144337567297406,-0.6,-0.25));
#24939=CARTESIAN_POINT('',(0.288675134594813,-0.6,0.));
#24940=CARTESIAN_POINT('',(0.144337567297406,-0.96,-0.25));
#24941=CARTESIAN_POINT('',(0.144337567297406,-0.6,-0.25));
#24942=CARTESIAN_POINT('',(0.288675134594813,-0.96,0.));
#24943=CARTESIAN_POINT('',(0.288675134594813,-0.96,0.));
#24944=CARTESIAN_POINT('',(0.288675134594813,-0.6,0.));
#24945=CARTESIAN_POINT('Origin',(-0.144337567297406,-0.6,-0.25));
#24946=CARTESIAN_POINT('',(-0.144337567297406,-0.6,-0.25));
#24947=CARTESIAN_POINT('',(0.144337567297406,-0.6,-0.25));
#24948=CARTESIAN_POINT('',(-0.144337567297406,-0.96,-0.25));
#24949=CARTESIAN_POINT('',(-0.144337567297406,-0.6,-0.25));
#24950=CARTESIAN_POINT('',(0.144337567297406,-0.96,-0.25));
#24951=CARTESIAN_POINT('Origin',(-0.288675134594813,-0.6,-8.32667268468867E-17));
#24952=CARTESIAN_POINT('',(-0.288675134594813,-0.6,-3.53525079574969E-17));
#24953=CARTESIAN_POINT('',(-0.144337567297406,-0.6,-0.25));
#24954=CARTESIAN_POINT('',(-0.288675134594813,-0.96,-5.55111512312578E-17));
#24955=CARTESIAN_POINT('',(-0.288675134594813,-0.6,-3.53525079574969E-17));
#24956=CARTESIAN_POINT('',(-0.144337567297406,-0.96,-0.25));
#24957=CARTESIAN_POINT('Origin',(-0.144337567297407,-0.6,0.25));
#24958=CARTESIAN_POINT('',(-0.144337567297407,-0.6,0.25));
#24959=CARTESIAN_POINT('',(-0.288675134594813,-0.6,-3.53525079574969E-17));
#24960=CARTESIAN_POINT('',(-0.144337567297407,-0.96,0.25));
#24961=CARTESIAN_POINT('',(-0.144337567297407,-0.6,0.25));
#24962=CARTESIAN_POINT('',(-0.288675134594813,-0.96,-3.53525079574969E-17));
#24963=CARTESIAN_POINT('Origin',(0.144337567297406,-0.6,0.25));
#24964=CARTESIAN_POINT('',(0.144337567297406,-0.6,0.25));
#24965=CARTESIAN_POINT('',(-0.144337567297407,-0.6,0.25));
#24966=CARTESIAN_POINT('',(0.144337567297406,-0.96,0.25));
#24967=CARTESIAN_POINT('',(0.144337567297406,-0.6,0.25));
#24968=CARTESIAN_POINT('',(-0.144337567297407,-0.96,0.25));
#24969=CARTESIAN_POINT('Origin',(0.288675134594813,-0.6,0.));
#24970=CARTESIAN_POINT('',(0.144337567297406,-0.6,0.25));
#24971=CARTESIAN_POINT('',(0.144337567297406,-0.96,0.25));
#24972=CARTESIAN_POINT('Origin',(0.,-0.6,0.));
#24973=CARTESIAN_POINT('Origin',(0.,-0.96,0.));
#25039=UNCERTAINTY_MEASURE_WITH_UNIT(LENGTH_MEASURE(0.001),#25075,
'DISTANCE_ACCURACY_VALUE',
'Maximum model space distance between geometric entities at asserted c
onnectivities');
#25040=UNCERTAINTY_MEASURE_WITH_UNIT(LENGTH_MEASURE(0.001),#25075,
'DISTANCE_ACCURACY_VALUE',
'Maximum model space distance between geometric entities at asserted c
onnectivities');
#25073=(
GEOMETRIC_REPRESENTATION_CONTEXT(3)
GLOBAL_UNCERTAINTY_ASSIGNED_CONTEXT((#25039))
GLOBAL_UNIT_ASSIGNED_CONTEXT((#25075,#25077,#25078))
REPRESENTATION_CONTEXT('','3D')
);
#25074=(
GEOMETRIC_REPRESENTATION_CONTEXT(3)
GLOBAL_UNCERTAINTY_ASSIGNED_CONTEXT((#25040))
GLOBAL_UNIT_ASSIGNED_CONTEXT((#25075,#25077,#25078))
REPRESENTATION_CONTEXT('','3D')
);
#25075=(
LENGTH_UNIT()
NAMED_UNIT(*)
SI_UNIT(.CENTI.,.METRE.)
);
#25077=(
NAMED_UNIT(*)
PLANE_ANGLE_UNIT()
SI_UNIT($,.RADIAN.)
);
#25078=(
NAMED_UNIT(*)
SI_UNIT($,.STERADIAN.)
SOLID_ANGLE_UNIT()
);
#25111=SHAPE_DEFINITION_REPRESENTATION(#25160,#25226);
#25160=PRODUCT_DEFINITION_SHAPE('',$,#25260);
#25226=SHAPE_REPRESENTATION('',(#9145),#25073);
#25227=PRODUCT_DEFINITION_CONTEXT('part definition',#25328,'design');
#25260=PRODUCT_DEFINITION('Cap Screw - M6x25','Cap Screw - M6x25',#25293,
#25227);
#25293=PRODUCT_DEFINITION_FORMATION('',$,#25362);
#25328=APPLICATION_CONTEXT(
'Core Data for Automotive Mechanical Design Process');
#25329=PRODUCT_CONTEXT('part definition',#25328,'mechanical');
#25362=PRODUCT('Cap Screw - M6x25','Cap Screw - M6x25',
'Cap Screw - M6x25',(#25329));
#25440=COLOUR_RGB('Black',0.12,0.14,0.17);
#25441=FILL_AREA_STYLE_COLOUR('',#25440);
#25442=FILL_AREA_STYLE('',(#25441));
#25443=SURFACE_STYLE_FILL_AREA(#25442);
#25444=SURFACE_SIDE_STYLE('',(#25443));
#25445=SURFACE_STYLE_USAGE(.BOTH.,#25444);
#25446=PRESENTATION_STYLE_ASSIGNMENT((#25445));
ENDSEC;
END-ISO-10303-21;
